ISO-10303-21;
HEADER;
FILE_DESCRIPTION (('STEP AP214'),
    '1' );
FILE_NAME ('socket head cap screw_iso_ISO 4762 M5 x 12 - 12N.step',
    '2026-10-03T12:29:21',
    ( '' ),
    ( '' ),
    'SwSTEP 2.0',
    'SolidWorks 2026',
    '' );
FILE_SCHEMA (( 'AUTOMOTIVE_DESIGN' ));
ENDSEC;

DATA;
#11=VERTEX_POINT ( 'NONE', #11628 ) ;
#21=ORIENTED_EDGE ( 'NONE', *, *, #4326, .F. ) ;
#37=DIRECTION ( 'NONE',  ( 0.000000000000000000, 0.000000000000000000, -1.000000000000000000 ) ) ;
#38=EDGE_CURVE ( 'NONE', #16141, #4659, #188, .T. ) ;
#71=DIRECTION ( 'NONE',  ( 0.000000000000000000, 0.000000000000000000, 1.000000000000000000 ) ) ;
#127=EDGE_CURVE ( 'NONE', #3649, #15600, #16319, .T. ) ;
#184=FACE_OUTER_BOUND ( 'NONE', #4764, .T. ) ;
#185=DIRECTION ( 'NONE',  ( 1.000000000000000000, 0.000000000000000000, 0.000000000000000000 ) ) ;
#188=LINE ( 'NONE', #16294, #20046 ) ;
#193=PLANE ( 'NONE',  #2937 ) ;
#207=DIRECTION ( 'NONE',  ( 0.000000000000000000, 0.000000000000000000, 1.000000000000000000 ) ) ;
#217=VECTOR ( 'NONE', #18691, 1000.000000000000000 ) ;
#226=EDGE_LOOP ( 'NONE', ( #12803, #12850, #13208, #16492, #13588 ) ) ;
#265=ORIENTED_EDGE ( 'NONE', *, *, #15414, .F. ) ;
#266=CARTESIAN_POINT ( 'NONE',  ( 5.000000000000004441, 5.204748896376250699E-16, -4.250000000000000000 ) ) ;
#301=EDGE_LOOP ( 'NONE', ( #6939, #11151, #11050, #12227 ) ) ;
#302=FACE_OUTER_BOUND ( 'NONE', #301, .T. ) ;
#313=UNCERTAINTY_MEASURE_WITH_UNIT (LENGTH_MEASURE( 1.000000000000000082E-05 ), #19598, 'distance_accuracy_value', 'NONE');
#318=DIRECTION ( 'NONE',  ( 0.000000000000000000, -0.4999999999999993894, 0.8660254037844389297 ) ) ;
#335=CARTESIAN_POINT ( 'NONE',  ( 2.500000000000000000, 2.357898499370433054, -1.951563910473907981E-15 ) ) ;
#356=ORIENTED_EDGE ( 'NONE', *, *, #13998, .F. ) ;
#364=LINE ( 'NONE', #2170, #17294 ) ;
#397=ORIENTED_EDGE ( 'NONE', *, *, #2654, .T. ) ;
#400=CARTESIAN_POINT ( 'NONE',  ( 16.55500000000001393, 0.000000000000000000, 0.000000000000000000 ) ) ;
#413=SURFACE_STYLE_USAGE ( .BOTH. , #8153 ) ;
#423=CIRCLE ( 'NONE', #18039, 2.500000000000000444 ) ;
#425=CARTESIAN_POINT ( 'NONE',  ( 5.200000000000002842, 0.000000000000000000, 0.000000000000000000 ) ) ;
#448=DIRECTION ( 'NONE',  ( 0.000000000000000000, -0.4999999999999993894, 0.8660254037844389297 ) ) ;
#463=ORIENTED_EDGE ( 'NONE', *, *, #15828, .T. ) ;
#482=EDGE_CURVE ( 'NONE', #14903, #18469, #1761, .T. ) ;
#514=CARTESIAN_POINT ( 'NONE',  ( 5.200000000000002842, 0.000000000000000000, 0.000000000000000000 ) ) ;
#537=EDGE_CURVE ( 'NONE', #13895, #14604, #14603, .T. ) ;
#599=ORIENTED_EDGE ( 'NONE', *, *, #3122, .F. ) ;
#609=AXIS2_PLACEMENT_3D ( 'NONE', #16709, #9927, #8437 ) ;
#707=AXIS2_PLACEMENT_3D ( 'NONE', #18906, #15601, #5958 ) ;
#746=CARTESIAN_POINT ( 'NONE',  ( 2.500000000000000000, 0.000000000000000000, 0.000000000000000000 ) ) ;
#748=( GEOMETRIC_REPRESENTATION_CONTEXT ( 3 ) GLOBAL_UNCERTAINTY_ASSIGNED_CONTEXT ( ( #20442 ) ) GLOBAL_UNIT_ASSIGNED_CONTEXT ( ( #18267, #8034, #11319 ) ) REPRESENTATION_CONTEXT ( 'NONE', 'WORKASPACE' ) );
#791=ORIENTED_EDGE ( 'NONE', *, *, #11962, .T. ) ;
#795=CARTESIAN_POINT ( 'NONE',  ( 2.500000000000000000, -2.357898499370432610, 3.252606517456513302E-15 ) ) ;
#800=CARTESIAN_POINT ( 'NONE',  ( 2.500000000000000000, -2.357898499370432610, 3.252606517456513302E-15 ) ) ;
#808=EDGE_CURVE ( 'NONE', #12190, #3649, #18001, .T. ) ;
#874=EDGE_LOOP ( 'NONE', ( #1892, #7772, #6301, #7238 ) ) ;
#954=EDGE_CURVE ( 'NONE', #11144, #2302, #1092, .T. ) ;
#1009=EDGE_CURVE ( 'NONE', #14849, #19012, #17928, .T. ) ;
#1069=VERTEX_POINT ( 'NONE', #16020 ) ;
#1092=LINE ( 'NONE', #18992, #4812 ) ;
#1111=DIRECTION ( 'NONE',  ( 0.000000000000000000, 0.000000000000000000, 1.000000000000000000 ) ) ;
#1118=CARTESIAN_POINT ( 'NONE',  ( 2.500000000000000000, 1.178949249685213863, -2.042000000000001148 ) ) ;
#1122=AXIS2_PLACEMENT_3D ( 'NONE', #5465, #6955, #2193 ) ;
#1215=AXIS2_PLACEMENT_3D ( 'NONE', #14046, #12549, #3215 ) ;
#1226=DIRECTION ( 'NONE',  ( -1.000000000000000000, -0.000000000000000000, -0.000000000000000000 ) ) ;
#1308=CARTESIAN_POINT ( 'NONE',  ( 2.500000000000000000, 1.178949249685218525, 2.041999999999999371 ) ) ;
#1349=CARTESIAN_POINT ( 'NONE',  ( 5.200000000000002842, 0.000000000000000000, 0.000000000000000000 ) ) ;
#1357=DIRECTION ( 'NONE',  ( -1.000000000000000000, -0.000000000000000000, -0.000000000000000000 ) ) ;
#1468=VERTEX_POINT ( 'NONE', #9321 ) ;
#1478=FILL_AREA_STYLE ('',( #6332 ) ) ;
#1498=CONICAL_SURFACE ( 'NONE', #4183, 2.055000000000000160, 0.7853981633974633780 ) ;
#1504=ORIENTED_EDGE ( 'NONE', *, *, #13362, .F. ) ;
#1534=CYLINDRICAL_SURFACE ( 'NONE', #20447, 4.250000000000000000 ) ;
#1535=DIRECTION ( 'NONE',  ( 0.000000000000000000, -0.8660254037844390407, -0.4999999999999994449 ) ) ;
#1540=COLOUR_RGB ( '', 0.31764706, 0.68627451, 0.89019608) ;
#1671=DIRECTION ( 'NONE',  ( 0.000000000000000000, 0.000000000000000000, 1.000000000000000000 ) ) ;
#1673=DIRECTION ( 'NONE',  ( 0.000000000000000000, 0.000000000000000000, 1.000000000000000000 ) ) ;
#1702=EDGE_CURVE ( 'NONE', #1069, #14401, #6749, .T. ) ;
#1749=TOROIDAL_SURFACE ( 'NONE', #7480, 4.000000000000000000, 0.2500000000000000000 ) ;
#1760=AXIS2_PLACEMENT_3D ( 'NONE', #5949, #17414, #4145 ) ;
#1761=LINE ( 'NONE', #16378, #8504 ) ;
#1846=ORIENTED_EDGE ( 'NONE', *, *, #13998, .T. ) ;
#1876=CARTESIAN_POINT ( 'NONE',  ( 2.500000000000000000, 0.000000000000000000, 0.000000000000000000 ) ) ;
#1892=ORIENTED_EDGE ( 'NONE', *, *, #16850, .F. ) ;
#1910=CARTESIAN_POINT ( 'NONE',  ( 2.500000000000000000, -1.178949249685213863, 2.042000000000002924 ) ) ;
#1936=DIRECTION ( 'NONE',  ( -1.000000000000000000, -0.000000000000000000, -0.000000000000000000 ) ) ;
#1970=CARTESIAN_POINT ( 'NONE',  ( 16.55500000000001393, 0.000000000000000000, 0.000000000000000000 ) ) ;
#1971=DIRECTION ( 'NONE',  ( 0.000000000000000000, 1.000000000000000000, -1.471414886128461471E-15 ) ) ;
#1983=PRODUCT_CONTEXT ( 'NONE', #7900, 'mechanical' ) ;
#1994=DIRECTION ( 'NONE',  ( 0.000000000000000000, -0.5000000000000012212, -0.8660254037844380415 ) ) ;
#2021=CARTESIAN_POINT ( 'NONE',  ( 2.500000000000000000, 1.178949249685213863, -2.042000000000001148 ) ) ;
#2023=ORIENTED_EDGE ( 'NONE', *, *, #19197, .F. ) ;
#2048=DIRECTION ( 'NONE',  ( -1.000000000000000000, -0.000000000000000000, -0.000000000000000000 ) ) ;
#2085=CARTESIAN_POINT ( 'NONE',  ( 5.000000000000004441, 0.000000000000000000, 4.250000000000000000 ) ) ;
#2093=DIRECTION ( 'NONE',  ( -0.5000000000000051070, 0.000000000000000000, 0.8660254037844355990 ) ) ;
#2132=LINE ( 'NONE', #15486, #10719 ) ;
#2170=CARTESIAN_POINT ( 'NONE',  ( 0.000000000000000000, -1.178949249685213863, 2.042000000000002924 ) ) ;
#2193=DIRECTION ( 'NONE',  ( 0.000000000000000000, 0.000000000000000000, 1.000000000000000000 ) ) ;
#2206=ORIENTED_EDGE ( 'NONE', *, *, #14142, .T. ) ;
#2302=VERTEX_POINT ( 'NONE', #17419 ) ;
#2318=PLANE ( 'NONE',  #7168 ) ;
#2331=ORIENTED_EDGE ( 'NONE', *, *, #20367, .F. ) ;
#2336=DIRECTION ( 'NONE',  ( -1.000000000000000000, -0.000000000000000000, -0.000000000000000000 ) ) ;
#2349=DIRECTION ( 'NONE',  ( 0.000000000000000000, 0.8660254037844380415, -0.5000000000000012212 ) ) ;
#2380=DIRECTION ( 'NONE',  ( -0.000000000000000000, 0.8660254037844390407, 0.4999999999999993339 ) ) ;
#2440=EDGE_CURVE ( 'NONE', #10418, #12190, #4876, .T. ) ;
#2447=AXIS2_PLACEMENT_3D ( 'NONE', #514, #18421, #13544 ) ;
#2487=EDGE_LOOP ( 'NONE', ( #9117, #16079, #3978, #3865, #20366 ) ) ;
#2502=AXIS2_PLACEMENT_3D ( 'NONE', #6469, #13161, #11251 ) ;
#2541=MECHANICAL_DESIGN_GEOMETRIC_PRESENTATION_REPRESENTATION('',(#20852),#12048);
#2565=CARTESIAN_POINT ( 'NONE',  ( 0.000000000000000000, 2.357898499370433054, -1.951563910473907981E-15 ) ) ;
#2586=CARTESIAN_POINT ( 'NONE',  ( 0.000000000000000000, 1.178949249685213863, -2.042000000000001148 ) ) ;
#2603=PLANE ( 'NONE',  #13126 ) ;
#2605=ORIENTED_EDGE ( 'NONE', *, *, #11547, .T. ) ;
#2617=EDGE_CURVE ( 'NONE', #13626, #14401, #18446, .T. ) ;
#2654=EDGE_CURVE ( 'NONE', #19812, #18469, #9965, .T. ) ;
#2696=FACE_OUTER_BOUND ( 'NONE', #6888, .T. ) ;
#2713=ORIENTED_EDGE ( 'NONE', *, *, #2855, .T. ) ;
#2718=DIRECTION ( 'NONE',  ( 0.000000000000000000, -0.5000000000000011102, -0.8660254037844379305 ) ) ;
#2760=ORIENTED_EDGE ( 'NONE', *, *, #2440, .T. ) ;
#2764=DIRECTION ( 'NONE',  ( -0.5000000000000051070, 1.060575238724903217E-16, -0.8660254037844355990 ) ) ;
#2826=CARTESIAN_POINT ( 'NONE',  ( 2.500000000000000000, -1.178949249685213863, 2.042000000000002924 ) ) ;
#2855=EDGE_CURVE ( 'NONE', #19557, #3608, #7853, .T. ) ;
#2915=ORIENTED_EDGE ( 'NONE', *, *, #13097, .F. ) ;
#2917=ORIENTED_EDGE ( 'NONE', *, *, #14896, .F. ) ;
#2924=CIRCLE ( 'NONE', #8006, 2.041999999999999815 ) ;
#2930=DIRECTION ( 'NONE',  ( -1.000000000000000000, -0.000000000000000000, -0.000000000000000000 ) ) ;
#2937=AXIS2_PLACEMENT_3D ( 'NONE', #14418, #16204, #6349 ) ;
#3102=FACE_OUTER_BOUND ( 'NONE', #11979, .T. ) ;
#3117=EDGE_CURVE ( 'NONE', #19897, #1468, #423, .T. ) ;
#3122=EDGE_CURVE ( 'NONE', #10495, #16164, #19056, .T. ) ;
#3150=ADVANCED_FACE ( 'NONE', ( #302 ), #18367, .F. ) ;
#3160=TOROIDAL_SURFACE ( 'NONE', #11960, 2.700000000000000622, 0.2000000000000000111 ) ;
#3175=AXIS2_PLACEMENT_3D ( 'NONE', #14733, #6454, #207 ) ;
#3215=DIRECTION ( 'NONE',  ( 0.000000000000000000, 0.000000000000000000, 1.000000000000000000 ) ) ;
#3256=FACE_OUTER_BOUND ( 'NONE', #2487, .T. ) ;
#3361=DIRECTION ( 'NONE',  ( 0.000000000000000000, 0.000000000000000000, 1.000000000000000000 ) ) ;
#3376=ORIENTED_EDGE ( 'NONE', *, *, #13097, .T. ) ;
#3381=DIRECTION ( 'NONE',  ( 0.000000000000000000, -1.000000000000000000, 1.287488025362403787E-15 ) ) ;
#3472=ORIENTED_EDGE ( 'NONE', *, *, #16669, .F. ) ;
#3608=VERTEX_POINT ( 'NONE', #11680 ) ;
#3612=LINE ( 'NONE', #335, #7941 ) ;
#3620=FACE_OUTER_BOUND ( 'NONE', #9347, .T. ) ;
#3641=ADVANCED_FACE ( 'NONE', ( #3620 ), #10852, .T. ) ;
#3649=VERTEX_POINT ( 'NONE', #10093 ) ;
#3669=FACE_OUTER_BOUND ( 'NONE', #874, .T. ) ;
#3700=ORIENTED_EDGE ( 'NONE', *, *, #13988, .F. ) ;
#3701=DIRECTION ( 'NONE',  ( 0.000000000000000000, -1.000000000000000000, 1.287488025362403787E-15 ) ) ;
#3828=ORIENTED_EDGE ( 'NONE', *, *, #15831, .T. ) ;
#3850=VECTOR ( 'NONE', #18373, 1000.000000000000000 ) ;
#3865=ORIENTED_EDGE ( 'NONE', *, *, #17779, .F. ) ;
#3918=AXIS2_PLACEMENT_3D ( 'NONE', #425, #5292, #19912 ) ;
#3978=ORIENTED_EDGE ( 'NONE', *, *, #1009, .F. ) ;
#4031=CARTESIAN_POINT ( 'NONE',  ( 0.000000000000000000, -1.178949249685218303, -2.041999999999998039 ) ) ;
#4057=AXIS2_PLACEMENT_3D ( 'NONE', #16449, #1936, #8393 ) ;
#4141=FACE_OUTER_BOUND ( 'NONE', #16696, .T. ) ;
#4145=DIRECTION ( 'NONE',  ( 0.000000000000000000, -1.224646799147353454E-16, 1.000000000000000000 ) ) ;
#4146=EDGE_LOOP ( 'NONE', ( #19786, #5788, #5231 ) ) ;
#4151=VECTOR ( 'NONE', #19677, 1000.000000000000000 ) ;
#4165=VECTOR ( 'NONE', #2764, 1000.000000000000114 ) ;
#4166=ADVANCED_FACE ( 'NONE', ( #9144 ), #16601, .F. ) ;
#4183=AXIS2_PLACEMENT_3D ( 'NONE', #6641, #16394, #11623 ) ;
#4213=ORIENTED_EDGE ( 'NONE', *, *, #13328, .F. ) ;
#4239=ORIENTED_EDGE ( 'NONE', *, *, #38, .T. ) ;
#4268=DIRECTION ( 'NONE',  ( 0.000000000000000000, 0.000000000000000000, 1.000000000000000000 ) ) ;
#4274=CARTESIAN_POINT ( 'NONE',  ( -31.74999999999995737, 0.000000000000000000, 0.000000000000000000 ) ) ;
#4326=EDGE_CURVE ( 'NONE', #6250, #1069, #5197, .T. ) ;
#4377=ADVANCED_FACE ( 'NONE', ( #19613 ), #1749, .T. ) ;
#4440=ORIENTED_EDGE ( 'NONE', *, *, #10028, .T. ) ;
#4448=CARTESIAN_POINT ( 'NONE',  ( 0.000000000000000000, 0.000000000000000000, 0.000000000000000000 ) ) ;
#4500=CARTESIAN_POINT ( 'NONE',  ( 5.000000000000002665, 0.000000000000000000, -2.700000000000000622 ) ) ;
#4509=DIRECTION ( 'NONE',  ( 0.000000000000000000, 0.000000000000000000, 1.000000000000000000 ) ) ;
#4515=LINE ( 'NONE', #17458, #11265 ) ;
#4588=FACE_OUTER_BOUND ( 'NONE', #4146, .T. ) ;
#4593=VECTOR ( 'NONE', #15721, 1000.000000000000114 ) ;
#4628=CARTESIAN_POINT ( 'NONE',  ( 2.500000000000000000, 0.000000000000000000, 0.000000000000000000 ) ) ;
#4648=CIRCLE ( 'NONE', #11087, 2.041999999999999815 ) ;
#4659=VERTEX_POINT ( 'NONE', #9437 ) ;
#4673=LINE ( 'NONE', #14217, #4165 ) ;
#4718=ORIENTED_EDGE ( 'NONE', *, *, #5202, .T. ) ;
#4731=DIRECTION ( 'NONE',  ( -1.000000000000000000, -0.000000000000000000, -0.000000000000000000 ) ) ;
#4752=ORIENTED_EDGE ( 'NONE', *, *, #18112, .F. ) ;
#4764=EDGE_LOOP ( 'NONE', ( #6815, #12237, #2023, #13533 ) ) ;
#4812=VECTOR ( 'NONE', #14227, 1000.000000000000000 ) ;
#4828=FACE_BOUND ( 'NONE', #17724, .T. ) ;
#4848=PRESENTATION_STYLE_ASSIGNMENT (( #11803 ) ) ;
#4876=CIRCLE ( 'NONE', #2502, 4.250000000000000000 ) ;
#4879=CARTESIAN_POINT ( 'NONE',  ( 0.2500000000000002220, 0.000000000000000000, 4.000000000000000000 ) ) ;
#4949=ORIENTED_EDGE ( 'NONE', *, *, #6075, .T. ) ;
#4960=AXIS2_PLACEMENT_3D ( 'NONE', #14391, #19351, #20834 ) ;
#4983=( NAMED_UNIT ( * ) PLANE_ANGLE_UNIT ( ) SI_UNIT ( $, .RADIAN. ) );
#5019=ORIENTED_EDGE ( 'NONE', *, *, #16399, .T. ) ;
#5047=DIRECTION ( 'NONE',  ( 0.000000000000000000, 0.000000000000000000, 1.000000000000000000 ) ) ;
#5111=ORIENTED_EDGE ( 'NONE', *, *, #14896, .T. ) ;
#5115=CARTESIAN_POINT ( 'NONE',  ( 2.500000000000000000, 2.357898499370433054, -1.951563910473907981E-15 ) ) ;
#5120=DIRECTION ( 'NONE',  ( 1.000000000000000000, 0.000000000000000000, 0.000000000000000000 ) ) ;
#5124=ORIENTED_EDGE ( 'NONE', *, *, #13362, .T. ) ;
#5143=DIRECTION ( 'NONE',  ( 0.000000000000000000, 0.000000000000000000, -1.000000000000000000 ) ) ;
#5197=LINE ( 'NONE', #19716, #18303 ) ;
#5202=EDGE_CURVE ( 'NONE', #14849, #5544, #17815, .T. ) ;
#5231=ORIENTED_EDGE ( 'NONE', *, *, #20217, .F. ) ;
#5292=DIRECTION ( 'NONE',  ( 1.000000000000000000, 0.000000000000000000, 0.000000000000000000 ) ) ;
#5313=AXIS2_PLACEMENT_3D ( 'NONE', #8424, #16581, #15504 ) ;
#5411=DIRECTION ( 'NONE',  ( 0.000000000000000000, -1.287488025362403787E-15, -1.000000000000000000 ) ) ;
#5436=DIRECTION ( 'NONE',  ( 0.000000000000000000, -0.5000000000000011102, -0.8660254037844379305 ) ) ;
#5465=CARTESIAN_POINT ( 'NONE',  ( 0.000000000000000000, 0.000000000000000000, 0.000000000000000000 ) ) ;
#5508=CARTESIAN_POINT ( 'NONE',  ( 17.00000000000000000, 2.516649172247811061E-16, -2.055000000000000160 ) ) ;
#5537=CIRCLE ( 'NONE', #10649, 4.250000000000000000 ) ;
#5544=VERTEX_POINT ( 'NONE', #6279 ) ;
#5612=ORIENTED_EDGE ( 'NONE', *, *, #15320, .F. ) ;
#5625=DIRECTION ( 'NONE',  ( 0.000000000000000000, 0.5000000000000012212, 0.8660254037844380415 ) ) ;
#5728=DIRECTION ( 'NONE',  ( -1.000000000000000000, -0.000000000000000000, -0.000000000000000000 ) ) ;
#5788=ORIENTED_EDGE ( 'NONE', *, *, #13299, .T. ) ;
#5798=DIRECTION ( 'NONE',  ( 0.000000000000000000, 0.000000000000000000, -1.000000000000000000 ) ) ;
#5804=UNCERTAINTY_MEASURE_WITH_UNIT (LENGTH_MEASURE( 1.000000000000000082E-05 ), #19495, 'distance_accuracy_value', 'NONE');
#5831=CLOSED_SHELL ( 'NONE', ( #7561, #4377, #3150, #11560, #10615, #16078, #16476, #14622, #3641, #20916, #17510, #15172, #9128, #9125, #9488, #8529, #7953, #19336, #18369, #18454, #6623, #19843, #8417, #14405, #20571, #12592, #4166 ) ) ;
#5872=CARTESIAN_POINT ( 'NONE',  ( -31.74999999999995737, 3.061616997868383634E-16, -2.500000000000000444 ) ) ;
#5881=AXIS2_PLACEMENT_3D ( 'NONE', #13178, #9785, #37 ) ;
#5905=EDGE_CURVE ( 'NONE', #10495, #12190, #2132, .T. ) ;
#5915=AXIS2_PLACEMENT_3D ( 'NONE', #13053, #17930, #16023 ) ;
#5949=CARTESIAN_POINT ( 'NONE',  ( 0.2500000000000002220, 4.898587196589412829E-16, -4.000000000000000000 ) ) ;
#5958=DIRECTION ( 'NONE',  ( 0.000000000000000000, 0.000000000000000000, 1.000000000000000000 ) ) ;
#5997=FACE_OUTER_BOUND ( 'NONE', #13404, .T. ) ;
#6004=CIRCLE ( 'NONE', #14815, 2.041999999999999815 ) ;
#6075=EDGE_CURVE ( 'NONE', #13895, #19557, #6640, .T. ) ;
#6091=FACE_OUTER_BOUND ( 'NONE', #14925, .T. ) ;
#6103=FACE_OUTER_BOUND ( 'NONE', #11895, .T. ) ;
#6115=FACE_BOUND ( 'NONE', #9162, .T. ) ;
#6156=CARTESIAN_POINT ( 'NONE',  ( 2.500000000000000000, -1.178949249685213863, 2.042000000000002924 ) ) ;
#6250=VERTEX_POINT ( 'NONE', #19797 ) ;
#6267=ORIENTED_EDGE ( 'NONE', *, *, #20217, .T. ) ;
#6279=CARTESIAN_POINT ( 'NONE',  ( 2.500000000000000000, 1.768423874527824902, 1.020999999999999019 ) ) ;
#6301=ORIENTED_EDGE ( 'NONE', *, *, #13988, .T. ) ;
#6332=FILL_AREA_STYLE_COLOUR ( '', #20363 ) ;
#6349=DIRECTION ( 'NONE',  ( 0.000000000000000000, 0.000000000000000000, -1.000000000000000000 ) ) ;
#6357=ORIENTED_EDGE ( 'NONE', *, *, #482, .T. ) ;
#6358=DIRECTION ( 'NONE',  ( 0.000000000000000000, 0.000000000000000000, -1.000000000000000000 ) ) ;
#6454=DIRECTION ( 'NONE',  ( 1.000000000000000000, 0.000000000000000000, 0.000000000000000000 ) ) ;
#6469=CARTESIAN_POINT ( 'NONE',  ( 0.2500000000000002220, 0.000000000000000000, 0.000000000000000000 ) ) ;
#6471=DIRECTION ( 'NONE',  ( 0.000000000000000000, 0.000000000000000000, 1.000000000000000000 ) ) ;
#6561=CARTESIAN_POINT ( 'NONE',  ( 2.500000000000000000, 1.178949249685213863, -2.042000000000001148 ) ) ;
#6568=LINE ( 'NONE', #11544, #10464 ) ;
#6623=ADVANCED_FACE ( 'NONE', ( #11509 ), #6734, .F. ) ;
#6640=CIRCLE ( 'NONE', #14111, 0.2000000000000000944 ) ;
#6641=CARTESIAN_POINT ( 'NONE',  ( 17.00000000000000000, 0.000000000000000000, 0.000000000000000000 ) ) ;
#6668=DIRECTION ( 'NONE',  ( 0.000000000000000000, 0.000000000000000000, -1.000000000000000000 ) ) ;
#6734=PLANE ( 'NONE',  #12791 ) ;
#6749=LINE ( 'NONE', #800, #4151 ) ;
#6815=ORIENTED_EDGE ( 'NONE', *, *, #16599, .T. ) ;
#6824=AXIS2_PLACEMENT_3D ( 'NONE', #18975, #10494, #16950 ) ;
#6827=ORIENTED_EDGE ( 'NONE', *, *, #2617, .F. ) ;
#6850=LINE ( 'NONE', #7062, #16828 ) ;
#6853=DIRECTION ( 'NONE',  ( -1.000000000000000000, -0.000000000000000000, -0.000000000000000000 ) ) ;
#6865=PRESENTATION_STYLE_ASSIGNMENT (( #413 ) ) ;
#6888=EDGE_LOOP ( 'NONE', ( #20590, #5612, #14863 ) ) ;
#6939=ORIENTED_EDGE ( 'NONE', *, *, #11333, .F. ) ;
#6955=DIRECTION ( 'NONE',  ( -1.000000000000000000, -0.000000000000000000, -0.000000000000000000 ) ) ;
#7062=CARTESIAN_POINT ( 'NONE',  ( 2.500000000000000000, 0.000000000000000000, 2.041999999999999815 ) ) ;
#7075=PRODUCT_DEFINITION_CONTEXT ( 'detailed design', #17252, 'design' ) ;
#7092=ORIENTED_EDGE ( 'NONE', *, *, #2617, .T. ) ;
#7094=DIRECTION ( 'NONE',  ( -1.000000000000000000, -0.000000000000000000, -0.000000000000000000 ) ) ;
#7168=AXIS2_PLACEMENT_3D ( 'NONE', #7611, #13870, #13660 ) ;
#7187=AXIS2_PLACEMENT_3D ( 'NONE', #15231, #15033, #13344 ) ;
#7193=ORIENTED_EDGE ( 'NONE', *, *, #11538, .F. ) ;
#7238=ORIENTED_EDGE ( 'NONE', *, *, #11333, .T. ) ;
#7253=ORIENTED_EDGE ( 'NONE', *, *, #14142, .F. ) ;
#7277=ORIENTED_EDGE ( 'NONE', *, *, #11504, .T. ) ;
#7322=CARTESIAN_POINT ( 'NONE',  ( 2.500000000000000000, 2.357898499370433054, -1.951563910473907981E-15 ) ) ;
#7352=EDGE_LOOP ( 'NONE', ( #21, #15886, #356 ) ) ;
#7357=DIRECTION ( 'NONE',  ( 0.000000000000000000, -0.4999999999999992784, 0.8660254037844389297 ) ) ;
#7391=CARTESIAN_POINT ( 'NONE',  ( 5.000000000000000888, 4.250000000000000000, 0.000000000000000000 ) ) ;
#7419=EDGE_CURVE ( 'NONE', #6250, #19812, #20376, .T. ) ;
#7464=ORIENTED_EDGE ( 'NONE', *, *, #16599, .F. ) ;
#7480=AXIS2_PLACEMENT_3D ( 'NONE', #19411, #11558, #6471 ) ;
#7494=PLANE ( 'NONE',  #8847 ) ;
#7552=VECTOR ( 'NONE', #19131, 1000.000000000000000 ) ;
#7560=ORIENTED_EDGE ( 'NONE', *, *, #18112, .T. ) ;
#7561=ADVANCED_FACE ( 'NONE', ( #9844 ), #17495, .F. ) ;
#7564=LINE ( 'NONE', #5872, #15578 ) ;
#7572=DIRECTION ( 'NONE',  ( 0.000000000000000000, 0.000000000000000000, 1.000000000000000000 ) ) ;
#7611=CARTESIAN_POINT ( 'NONE',  ( 2.500000000000000000, 2.357898499370433054, -1.951563910473907981E-15 ) ) ;
#7715=AXIS2_PLACEMENT_3D ( 'NONE', #19850, #2048, #18262 ) ;
#7725=CARTESIAN_POINT ( 'NONE',  ( 2.500000000000000000, -1.178949249685213863, 2.042000000000002924 ) ) ;
#7745=DIRECTION ( 'NONE',  ( 0.000000000000000000, -1.000000000000000000, 0.000000000000000000 ) ) ;
#7772=ORIENTED_EDGE ( 'NONE', *, *, #3117, .T. ) ;
#7853=CIRCLE ( 'NONE', #6824, 2.700000000000000622 ) ;
#7858=ORIENTED_EDGE ( 'NONE', *, *, #15727, .F. ) ;
#7877=CARTESIAN_POINT ( 'NONE',  ( 0.000000000000000000, 1.178949249685218525, 2.041999999999999371 ) ) ;
#7900=APPLICATION_CONTEXT ( 'automotive_design' ) ;
#7941=VECTOR ( 'NONE', #448, 1000.000000000000114 ) ;
#7953=ADVANCED_FACE ( 'NONE', ( #15211 ), #8958, .T. ) ;
#7955=CARTESIAN_POINT ( 'NONE',  ( 5.200000000000002842, 0.000000000000000000, -2.700000000000000622 ) ) ;
#8006=AXIS2_PLACEMENT_3D ( 'NONE', #4628, #4731, #20937 ) ;
#8025=LINE ( 'NONE', #11797, #16171 ) ;
#8034=( NAMED_UNIT ( * ) PLANE_ANGLE_UNIT ( ) SI_UNIT ( $, .RADIAN. ) );
#8144=ORIENTED_EDGE ( 'NONE', *, *, #3117, .F. ) ;
#8147=CIRCLE ( 'NONE', #19312, 2.055000000000000160 ) ;
#8153=SURFACE_SIDE_STYLE ('',( #14937 ) ) ;
#8177=ORIENTED_EDGE ( 'NONE', *, *, #127, .F. ) ;
#8197=ORIENTED_EDGE ( 'NONE', *, *, #7419, .F. ) ;
#8237=VECTOR ( 'NONE', #3701, 1000.000000000000000 ) ;
#8290=FACE_OUTER_BOUND ( 'NONE', #7352, .T. ) ;
#8294=CARTESIAN_POINT ( 'NONE',  ( 5.200000000000002842, 0.000000000000000000, 0.000000000000000000 ) ) ;
#8314=CARTESIAN_POINT ( 'NONE',  ( 0.000000000000000000, 0.000000000000000000, 0.000000000000000000 ) ) ;
#8333=VECTOR ( 'NONE', #2336, 1000.000000000000000 ) ;
#8338=AXIS2_PLACEMENT_3D ( 'NONE', #14731, #8456, #19798 ) ;
#8393=DIRECTION ( 'NONE',  ( 0.000000000000000000, 0.000000000000000000, 1.000000000000000000 ) ) ;
#8395=CARTESIAN_POINT ( 'NONE',  ( 5.200000000000002842, 0.000000000000000000, 2.500000000000000444 ) ) ;
#8412=ORIENTED_EDGE ( 'NONE', *, *, #16669, .T. ) ;
#8417=ADVANCED_FACE ( 'NONE', ( #17262 ), #2318, .F. ) ;
#8424=CARTESIAN_POINT ( 'NONE',  ( 5.200000000000002842, 3.306546357697854226E-16, 2.700000000000000622 ) ) ;
#8437=DIRECTION ( 'NONE',  ( 0.000000000000000000, 0.000000000000000000, 1.000000000000000000 ) ) ;
#8456=DIRECTION ( 'NONE',  ( -1.000000000000000000, -0.000000000000000000, -0.000000000000000000 ) ) ;
#8479=ORIENTED_EDGE ( 'NONE', *, *, #3122, .T. ) ;
#8504=VECTOR ( 'NONE', #19250, 1000.000000000000000 ) ;
#8508=DIRECTION ( 'NONE',  ( 0.000000000000000000, 0.000000000000000000, -1.000000000000000000 ) ) ;
#8529=ADVANCED_FACE ( 'NONE', ( #3256 ), #19363, .F. ) ;
#8642=DIRECTION ( 'NONE',  ( -1.000000000000000000, -0.000000000000000000, -0.000000000000000000 ) ) ;
#8705=CIRCLE ( 'NONE', #9353, 2.500000000000000444 ) ;
#8713=EDGE_CURVE ( 'NONE', #17642, #14849, #12632, .T. ) ;
#8779=EDGE_LOOP ( 'NONE', ( #13623, #15817, #7253, #18379 ) ) ;
#8847=AXIS2_PLACEMENT_3D ( 'NONE', #7391, #13977, #5798 ) ;
#8893=ORIENTED_EDGE ( 'NONE', *, *, #20402, .F. ) ;
#8958=PLANE ( 'NONE',  #20373 ) ;
#9045=CARTESIAN_POINT ( 'NONE',  ( 2.500000000000000000, 0.000000000000000000, 0.000000000000000000 ) ) ;
#9117=ORIENTED_EDGE ( 'NONE', *, *, #11676, .T. ) ;
#9125=ADVANCED_FACE ( 'NONE', ( #5997 ), #19734, .T. ) ;
#9128=ADVANCED_FACE ( 'NONE', ( #6091 ), #3160, .F. ) ;
#9129=LINE ( 'NONE', #14330, #12928 ) ;
#9144=FACE_OUTER_BOUND ( 'NONE', #19169, .T. ) ;
#9162=EDGE_LOOP ( 'NONE', ( #2713, #12816 ) ) ;
#9209=STYLED_ITEM ( 'NONE', ( #4848 ), #17543 ) ;
#9241=VERTEX_POINT ( 'NONE', #16475 ) ;
#9259=LINE ( 'NONE', #13925, #4593 ) ;
#9282=AXIS2_PLACEMENT_3D ( 'NONE', #18914, #1535, #17432 ) ;
#9321=CARTESIAN_POINT ( 'NONE',  ( 16.55500000000001393, 0.000000000000000000, 2.500000000000000444 ) ) ;
#9347=EDGE_LOOP ( 'NONE', ( #265, #19293, #11692, #8144 ) ) ;
#9353=AXIS2_PLACEMENT_3D ( 'NONE', #1970, #13204, #19653 ) ;
#9406=CARTESIAN_POINT ( 'NONE',  ( -31.74999999999995737, 0.000000000000000000, 0.000000000000000000 ) ) ;
#9437=CARTESIAN_POINT ( 'NONE',  ( 2.500000000000000000, 1.178949249685213863, -2.042000000000001148 ) ) ;
#9448=LINE ( 'NONE', #1308, #11709 ) ;
#9472=ORIENTED_EDGE ( 'NONE', *, *, #1702, .F. ) ;
#9488=ADVANCED_FACE ( 'NONE', ( #15725 ), #20595, .T. ) ;
#9508=CARTESIAN_POINT ( 'NONE',  ( 2.500000000000000000, 0.000000000000000000, 0.000000000000000000 ) ) ;
#9553=FACE_OUTER_BOUND ( 'NONE', #20631, .T. ) ;
#9558=PLANE ( 'NONE',  #17869 ) ;
#9574=AXIS2_PLACEMENT_3D ( 'NONE', #1876, #8642, #5047 ) ;
#9785=DIRECTION ( 'NONE',  ( 1.000000000000000000, 0.000000000000000000, 0.000000000000000000 ) ) ;
#9817=DIRECTION ( 'NONE',  ( 1.000000000000000000, 0.000000000000000000, 0.000000000000000000 ) ) ;
#9844=FACE_OUTER_BOUND ( 'NONE', #12976, .T. ) ;
#9879=DIRECTION ( 'NONE',  ( 0.000000000000000000, -0.4999999999999993894, 0.8660254037844389297 ) ) ;
#9912=AXIS2_PLACEMENT_3D ( 'NONE', #8314, #14495, #20932 ) ;
#9914=DIRECTION ( 'NONE',  ( -1.000000000000000000, -0.000000000000000000, -0.000000000000000000 ) ) ;
#9927=DIRECTION ( 'NONE',  ( -1.000000000000000000, -0.000000000000000000, -0.000000000000000000 ) ) ;
#9965=LINE ( 'NONE', #16429, #17052 ) ;
#9987=FACE_OUTER_BOUND ( 'NONE', #15422, .T. ) ;
#10020=LINE ( 'NONE', #16488, #12761 ) ;
#10028=EDGE_CURVE ( 'NONE', #17230, #14903, #9129, .T. ) ;
#10093=CARTESIAN_POINT ( 'NONE',  ( 0.000000000000000000, 5.051668046482832750E-16, -4.000000000000000000 ) ) ;
#10119=CARTESIAN_POINT ( 'NONE',  ( 17.00000000000000000, 0.000000000000000000, 0.000000000000000000 ) ) ;
#10162=( NAMED_UNIT ( * ) SI_UNIT ( $, .STERADIAN. ) SOLID_ANGLE_UNIT ( ) );
#10262=CIRCLE ( 'NONE', #20412, 4.000000000000000000 ) ;
#10346=PRODUCT ( 'socket head cap screw_iso_ISO 4762 M5 x 12 - 12N', 'socket head cap screw_iso_ISO 4762 M5 x 12 - 12N', '', ( #1983 ) ) ;
#10412=FACE_OUTER_BOUND ( 'NONE', #13783, .T. ) ;
#10418=VERTEX_POINT ( 'NONE', #11809 ) ;
#10464=VECTOR ( 'NONE', #318, 1000.000000000000114 ) ;
#10494=DIRECTION ( 'NONE',  ( -1.000000000000000000, -0.000000000000000000, -0.000000000000000000 ) ) ;
#10495=VERTEX_POINT ( 'NONE', #266 ) ;
#10509=PLANE ( 'NONE',  #17636 ) ;
#10615=ADVANCED_FACE ( 'NONE', ( #12448 ), #12870, .T. ) ;
#10641=VERTEX_POINT ( 'NONE', #7877 ) ;
#10648=CARTESIAN_POINT ( 'NONE',  ( 2.500000000000000000, -1.178949249685218303, -2.041999999999998039 ) ) ;
#10649=AXIS2_PLACEMENT_3D ( 'NONE', #14162, #19135, #7572 ) ;
#10708=PRODUCT_DEFINITION_SHAPE ( 'NONE', 'NONE',  #19582 ) ;
#10719=VECTOR ( 'NONE', #7094, 1000.000000000000000 ) ;
#10723=VECTOR ( 'NONE', #2718, 1000.000000000000114 ) ;
#10744=ORIENTED_EDGE ( 'NONE', *, *, #10864, .T. ) ;
#10761=CIRCLE ( 'NONE', #7715, 2.700000000000000622 ) ;
#10763=DIRECTION ( 'NONE',  ( 1.000000000000000000, 0.000000000000000000, 0.000000000000000000 ) ) ;
#10772=CARTESIAN_POINT ( 'NONE',  ( 2.500000000000000000, -1.178949249685213863, 2.042000000000002924 ) ) ;
#10817=ORIENTED_EDGE ( 'NONE', *, *, #11547, .F. ) ;
#10852=CONICAL_SURFACE ( 'NONE', #4057, 2.055000000000000160, 0.7853981633974633780 ) ;
#10864=EDGE_CURVE ( 'NONE', #17642, #6250, #9259, .T. ) ;
#10987=CYLINDRICAL_SURFACE ( 'NONE', #13077, 4.250000000000000000 ) ;
#11016=SHAPE_REPRESENTATION ( 'socket head cap screw_iso_ISO 4762 M5 x 12 - 12N', ( #12461 ), #19129 ) ;
#11023=EDGE_CURVE ( 'NONE', #19012, #10641, #9448, .T. ) ;
#11050=ORIENTED_EDGE ( 'NONE', *, *, #2855, .F. ) ;
#11073=DIRECTION ( 'NONE',  ( -1.000000000000000000, -0.000000000000000000, -0.000000000000000000 ) ) ;
#11074=DIRECTION ( 'NONE',  ( 0.000000000000000000, 0.000000000000000000, -1.000000000000000000 ) ) ;
#11087=AXIS2_PLACEMENT_3D ( 'NONE', #13009, #9914, #1673 ) ;
#11144=VERTEX_POINT ( 'NONE', #1910 ) ;
#11151=ORIENTED_EDGE ( 'NONE', *, *, #20367, .T. ) ;
#11169=LINE ( 'NONE', #1118, #15696 ) ;
#11193=CARTESIAN_POINT ( 'NONE',  ( 2.500000000000000000, -1.178949249685213863, 2.042000000000002924 ) ) ;
#11251=DIRECTION ( 'NONE',  ( 0.000000000000000000, 0.000000000000000000, 1.000000000000000000 ) ) ;
#11265=VECTOR ( 'NONE', #2930, 1000.000000000000000 ) ;
#11273=EDGE_LOOP ( 'NONE', ( #18084, #599 ) ) ;
#11281=ORIENTED_EDGE ( 'NONE', *, *, #4326, .T. ) ;
#11294=PLANE ( 'NONE',  #9912 ) ;
#11303=LINE ( 'NONE', #2826, #10723 ) ;
#11319=( NAMED_UNIT ( * ) SI_UNIT ( $, .STERADIAN. ) SOLID_ANGLE_UNIT ( ) );
#11333=EDGE_CURVE ( 'NONE', #14604, #13895, #17838, .T. ) ;
#11349=DIRECTION ( 'NONE',  ( 0.000000000000000000, -1.000000000000000000, 0.000000000000000000 ) ) ;
#11408=CIRCLE ( 'NONE', #5313, 0.2000000000000000944 ) ;
#11495=ORIENTED_EDGE ( 'NONE', *, *, #808, .F. ) ;
#11504=EDGE_CURVE ( 'NONE', #13626, #1069, #2924, .T. ) ;
#11509=FACE_OUTER_BOUND ( 'NONE', #20284, .T. ) ;
#11522=CARTESIAN_POINT ( 'NONE',  ( 16.55500000000001393, 3.061616997868383634E-16, -2.500000000000000444 ) ) ;
#11538=EDGE_CURVE ( 'NONE', #9241, #11681, #16806, .T. ) ;
#11544=CARTESIAN_POINT ( 'NONE',  ( 2.500000000000000000, 2.357898499370433054, -1.951563910473907981E-15 ) ) ;
#11547=EDGE_CURVE ( 'NONE', #11144, #17642, #11303, .T. ) ;
#11549=ORIENTED_EDGE ( 'NONE', *, *, #482, .F. ) ;
#11552=PLANE ( 'NONE',  #5915 ) ;
#11558=DIRECTION ( 'NONE',  ( -1.000000000000000000, -0.000000000000000000, -0.000000000000000000 ) ) ;
#11560=ADVANCED_FACE ( 'NONE', ( #6103 ), #10987, .T. ) ;
#11584=EDGE_LOOP ( 'NONE', ( #2206, #12354 ) ) ;
#11623=DIRECTION ( 'NONE',  ( 0.000000000000000000, 0.000000000000000000, 1.000000000000000000 ) ) ;
#11625=CYLINDRICAL_SURFACE ( 'NONE', #609, 2.500000000000000444 ) ;
#11628=CARTESIAN_POINT ( 'NONE',  ( 3.678949249685231848, 5.299604027854762026E-17, 0.000000000000000000 ) ) ;
#11647=FILL_AREA_STYLE_COLOUR ( '', #1540 ) ;
#11676=EDGE_CURVE ( 'NONE', #2302, #10641, #10020, .T. ) ;
#11680=CARTESIAN_POINT ( 'NONE',  ( 5.000000000000002665, 3.306546357697854226E-16, 2.700000000000000622 ) ) ;
#11681=VERTEX_POINT ( 'NONE', #11833 ) ;
#11692=ORIENTED_EDGE ( 'NONE', *, *, #14449, .T. ) ;
#11701=SURFACE_SIDE_STYLE ('',( #13407 ) ) ;
#11709=VECTOR ( 'NONE', #5728, 1000.000000000000000 ) ;
#11757=( NAMED_UNIT ( * ) PLANE_ANGLE_UNIT ( ) SI_UNIT ( $, .RADIAN. ) );
#11797=CARTESIAN_POINT ( 'NONE',  ( -31.74999999999995737, 0.000000000000000000, 4.250000000000000000 ) ) ;
#11803=SURFACE_STYLE_USAGE ( .BOTH. , #11701 ) ;
#11809=CARTESIAN_POINT ( 'NONE',  ( 0.2500000000000002220, 0.000000000000000000, 4.250000000000000000 ) ) ;
#11833=CARTESIAN_POINT ( 'NONE',  ( 17.00000000000000000, 0.000000000000000000, 2.055000000000000160 ) ) ;
#11895=EDGE_LOOP ( 'NONE', ( #791, #20653, #463, #1504 ) ) ;
#11901=MECHANICAL_DESIGN_GEOMETRIC_PRESENTATION_REPRESENTATION('',(#9209),#748);
#11960=AXIS2_PLACEMENT_3D ( 'NONE', #1349, #5120, #8508 ) ;
#11962=EDGE_CURVE ( 'NONE', #16164, #10495, #5537, .T. ) ;
#11979=EDGE_LOOP ( 'NONE', ( #20214, #8479, #5124, #2760 ) ) ;
#11995=DIRECTION ( 'NONE',  ( 0.000000000000000000, 1.000000000000000000, -1.287488025362403787E-15 ) ) ;
#12048=( GEOMETRIC_REPRESENTATION_CONTEXT ( 3 ) GLOBAL_UNCERTAINTY_ASSIGNED_CONTEXT ( ( #5804 ) ) GLOBAL_UNIT_ASSIGNED_CONTEXT ( ( #19495, #11757, #16618 ) ) REPRESENTATION_CONTEXT ( 'NONE', 'WORKASPACE' ) );
#12190=VERTEX_POINT ( 'NONE', #18158 ) ;
#12211=ORIENTED_EDGE ( 'NONE', *, *, #15727, .T. ) ;
#12227=ORIENTED_EDGE ( 'NONE', *, *, #6075, .F. ) ;
#12237=ORIENTED_EDGE ( 'NONE', *, *, #15414, .T. ) ;
#12294=AXIS2_PLACEMENT_3D ( 'NONE', #20601, #10763, #11074 ) ;
#12300=DIRECTION ( 'NONE',  ( 0.000000000000000000, 0.000000000000000000, 1.000000000000000000 ) ) ;
#12329=DIRECTION ( 'NONE',  ( -1.000000000000000000, -0.000000000000000000, -0.000000000000000000 ) ) ;
#12354=ORIENTED_EDGE ( 'NONE', *, *, #127, .T. ) ;
#12436=DIRECTION ( 'NONE',  ( 1.000000000000000000, 0.000000000000000000, 0.000000000000000000 ) ) ;
#12448=FACE_OUTER_BOUND ( 'NONE', #17394, .T. ) ;
#12453=LINE ( 'NONE', #17225, #7552 ) ;
#12461=AXIS2_PLACEMENT_3D ( 'NONE', #19474, #3361, #185 ) ;
#12515=DIRECTION ( 'NONE',  ( -1.000000000000000000, -0.000000000000000000, -0.000000000000000000 ) ) ;
#12549=DIRECTION ( 'NONE',  ( -1.000000000000000000, -0.000000000000000000, -0.000000000000000000 ) ) ;
#12568=CARTESIAN_POINT ( 'NONE',  ( 0.2500000000000002220, 0.000000000000000000, 0.000000000000000000 ) ) ;
#12592=ADVANCED_FACE ( 'NONE', ( #9553 ), #11552, .F. ) ;
#12632=CIRCLE ( 'NONE', #9574, 2.041999999999999815 ) ;
#12678=CIRCLE ( 'NONE', #3175, 4.250000000000000000 ) ;
#12761=VECTOR ( 'NONE', #1971, 1000.000000000000000 ) ;
#12768=CIRCLE ( 'NONE', #19851, 2.041999999999999815 ) ;
#12791=AXIS2_PLACEMENT_3D ( 'NONE', #17983, #9817, #5143 ) ;
#12803=ORIENTED_EDGE ( 'NONE', *, *, #16929, .F. ) ;
#12816=ORIENTED_EDGE ( 'NONE', *, *, #13328, .T. ) ;
#12850=ORIENTED_EDGE ( 'NONE', *, *, #16399, .F. ) ;
#12870=CYLINDRICAL_SURFACE ( 'NONE', #1215, 2.500000000000000444 ) ;
#12902=AXIS2_PLACEMENT_3D ( 'NONE', #7322, #2349, #5625 ) ;
#12928=VECTOR ( 'NONE', #17508, 999.9999999999998863 ) ;
#12974=PLANE ( 'NONE',  #5881 ) ;
#12976=EDGE_LOOP ( 'NONE', ( #2915, #13517, #7277, #1846, #18564 ) ) ;
#12977=DIRECTION ( 'NONE',  ( 1.000000000000000000, 0.000000000000000000, 0.000000000000000000 ) ) ;
#12989=AXIS2_PLACEMENT_3D ( 'NONE', #12568, #19034, #4509 ) ;
#13009=CARTESIAN_POINT ( 'NONE',  ( 2.500000000000000000, 0.000000000000000000, 0.000000000000000000 ) ) ;
#13040=FILL_AREA_STYLE ('',( #11647 ) ) ;
#13053=CARTESIAN_POINT ( 'NONE',  ( 2.500000000000000000, 2.357898499370433054, -1.951563910473907981E-15 ) ) ;
#13077=AXIS2_PLACEMENT_3D ( 'NONE', #9406, #1357, #1671 ) ;
#13079=DIRECTION ( 'NONE',  ( 0.000000000000000000, 0.000000000000000000, -1.000000000000000000 ) ) ;
#13097=EDGE_CURVE ( 'NONE', #11, #14849, #6850, .T. ) ;
#13126=AXIS2_PLACEMENT_3D ( 'NONE', #795, #2380, #7357 ) ;
#13161=DIRECTION ( 'NONE',  ( 1.000000000000000000, 0.000000000000000000, 0.000000000000000000 ) ) ;
#13178=CARTESIAN_POINT ( 'NONE',  ( 17.00000000000000000, 2.055000000000000160, 0.000000000000000000 ) ) ;
#13204=DIRECTION ( 'NONE',  ( -1.000000000000000000, -0.000000000000000000, -0.000000000000000000 ) ) ;
#13208=ORIENTED_EDGE ( 'NONE', *, *, #18651, .T. ) ;
#13264=DIRECTION ( 'NONE',  ( 0.000000000000000000, 0.4999999999999993339, -0.8660254037844390407 ) ) ;
#13282=ORIENTED_EDGE ( 'NONE', *, *, #8713, .F. ) ;
#13299=EDGE_CURVE ( 'NONE', #18355, #16141, #19638, .T. ) ;
#13328=EDGE_CURVE ( 'NONE', #3608, #19557, #10761, .T. ) ;
#13344=DIRECTION ( 'NONE',  ( 0.000000000000000000, 0.000000000000000000, 1.000000000000000000 ) ) ;
#13349=ORIENTED_EDGE ( 'NONE', *, *, #13299, .F. ) ;
#13362=EDGE_CURVE ( 'NONE', #16164, #10418, #8025, .T. ) ;
#13391=CARTESIAN_POINT ( 'NONE',  ( 2.500000000000000000, 3.004629197474318851E-15, 2.042000000000000259 ) ) ;
#13404=EDGE_LOOP ( 'NONE', ( #11495, #15388, #3828, #8177 ) ) ;
#13407=SURFACE_STYLE_FILL_AREA ( #1478 ) ;
#13415=DIRECTION ( 'NONE',  ( -1.000000000000000000, -0.000000000000000000, -0.000000000000000000 ) ) ;
#13460=SHAPE_REPRESENTATION_RELATIONSHIP ( 'NONE' , 'NONE' ,  #11016, #16501 ) ;
#13465=VECTOR ( 'NONE', #18062, 999.9999999999998863 ) ;
#13517=ORIENTED_EDGE ( 'NONE', *, *, #15582, .T. ) ;
#13523=DIRECTION ( 'NONE',  ( 0.000000000000000000, 0.8660254037844380415, -0.5000000000000011102 ) ) ;
#13533=ORIENTED_EDGE ( 'NONE', *, *, #14449, .F. ) ;
#13544=DIRECTION ( 'NONE',  ( 0.000000000000000000, 0.000000000000000000, -1.000000000000000000 ) ) ;
#13569=DIRECTION ( 'NONE',  ( 0.000000000000000000, 0.4999999999999993339, -0.8660254037844390407 ) ) ;
#13584=CARTESIAN_POINT ( 'NONE',  ( 2.500000000000000000, 1.178949249685213863, -2.042000000000001148 ) ) ;
#13588=ORIENTED_EDGE ( 'NONE', *, *, #11023, .T. ) ;
#13623=ORIENTED_EDGE ( 'NONE', *, *, #15828, .F. ) ;
#13626=VERTEX_POINT ( 'NONE', #20482 ) ;
#13660=DIRECTION ( 'NONE',  ( 0.000000000000000000, 0.000000000000000000, -1.000000000000000000 ) ) ;
#13672=VECTOR ( 'NONE', #3381, 1000.000000000000000 ) ;
#13683=DIRECTION ( 'NONE',  ( 0.000000000000000000, 0.000000000000000000, 1.000000000000000000 ) ) ;
#13716=PRODUCT_DEFINITION_FORMATION_WITH_SPECIFIED_SOURCE ( 'ANY', '', #10346, .NOT_KNOWN. ) ;
#13721=DIRECTION ( 'NONE',  ( 0.000000000000000000, 0.000000000000000000, 1.000000000000000000 ) ) ;
#13783=EDGE_LOOP ( 'NONE', ( #4440, #4752, #19019, #13349, #5019 ) ) ;
#13801=LINE ( 'NONE', #5508, #18729 ) ;
#13870=DIRECTION ( 'NONE',  ( 1.000000000000000000, 0.000000000000000000, 0.000000000000000000 ) ) ;
#13895=VERTEX_POINT ( 'NONE', #16751 ) ;
#13925=CARTESIAN_POINT ( 'NONE',  ( 2.500000000000000000, -1.178949249685213863, 2.042000000000002924 ) ) ;
#13977=DIRECTION ( 'NONE',  ( 1.000000000000000000, 0.000000000000000000, 0.000000000000000000 ) ) ;
#13988=EDGE_CURVE ( 'NONE', #1468, #14604, #15483, .T. ) ;
#13998=EDGE_CURVE ( 'NONE', #1069, #17642, #12768, .T. ) ;
#14009=CARTESIAN_POINT ( 'NONE',  ( 0.000000000000000000, 0.000000000000000000, 4.000000000000000000 ) ) ;
#14038=CARTESIAN_POINT ( 'NONE',  ( 2.500000000000000000, -2.357898499370432610, 3.252606517456513302E-15 ) ) ;
#14046=CARTESIAN_POINT ( 'NONE',  ( -31.74999999999995737, 0.000000000000000000, 0.000000000000000000 ) ) ;
#14111=AXIS2_PLACEMENT_3D ( 'NONE', #7955, #7745, #6358 ) ;
#14142=EDGE_CURVE ( 'NONE', #15600, #3649, #10262, .T. ) ;
#14162=CARTESIAN_POINT ( 'NONE',  ( 5.000000000000004441, 0.000000000000000000, 0.000000000000000000 ) ) ;
#14186=ORIENTED_EDGE ( 'NONE', *, *, #19197, .T. ) ;
#14217=CARTESIAN_POINT ( 'NONE',  ( 2.500000000000000000, 2.500728763858895382E-16, -2.041999999999999815 ) ) ;
#14227=DIRECTION ( 'NONE',  ( -1.000000000000000000, -0.000000000000000000, -0.000000000000000000 ) ) ;
#14296=DIRECTION ( 'NONE',  ( -0.000000000000000000, 1.471414886128461471E-15, 1.000000000000000000 ) ) ;
#14330=CARTESIAN_POINT ( 'NONE',  ( 0.000000000000000000, 2.357898499370433054, -1.951563910473907981E-15 ) ) ;
#14360=ORIENTED_EDGE ( 'NONE', *, *, #17779, .T. ) ;
#14391=CARTESIAN_POINT ( 'NONE',  ( 17.00000000000000000, 0.000000000000000000, 0.000000000000000000 ) ) ;
#14401=VERTEX_POINT ( 'NONE', #20499 ) ;
#14405=ADVANCED_FACE ( 'NONE', ( #2696 ), #18813, .F. ) ;
#14418=CARTESIAN_POINT ( 'NONE',  ( 2.500000000000000000, 2.357898499370433054, -1.951563910473907981E-15 ) ) ;
#14432=LINE ( 'NONE', #6561, #13672 ) ;
#14449=EDGE_CURVE ( 'NONE', #11681, #1468, #12453, .T. ) ;
#14495=DIRECTION ( 'NONE',  ( -1.000000000000000000, 0.000000000000000000, -0.000000000000000000 ) ) ;
#14565=LINE ( 'NONE', #20694, #17959 ) ;
#14603=CIRCLE ( 'NONE', #18664, 2.500000000000000444 ) ;
#14604=VERTEX_POINT ( 'NONE', #8395 ) ;
#14622=ADVANCED_FACE ( 'NONE', ( #9987 ), #12974, .T. ) ;
#14630=AXIS2_PLACEMENT_3D ( 'NONE', #7725, #14296, #20848 ) ;
#14731=CARTESIAN_POINT ( 'NONE',  ( 2.500000000000000000, 0.000000000000000000, 0.000000000000000000 ) ) ;
#14733=CARTESIAN_POINT ( 'NONE',  ( 0.2500000000000002220, 0.000000000000000000, 0.000000000000000000 ) ) ;
#14806=DIRECTION ( 'NONE',  ( -1.000000000000000000, -0.000000000000000000, -0.000000000000000000 ) ) ;
#14813=SHAPE_DEFINITION_REPRESENTATION ( #10708, #11016 ) ;
#14815=AXIS2_PLACEMENT_3D ( 'NONE', #9045, #12329, #4268 ) ;
#14849=VERTEX_POINT ( 'NONE', #13391 ) ;
#14863=ORIENTED_EDGE ( 'NONE', *, *, #5202, .F. ) ;
#14896=EDGE_CURVE ( 'NONE', #14401, #18469, #20378, .T. ) ;
#14903=VERTEX_POINT ( 'NONE', #2586 ) ;
#14925=EDGE_LOOP ( 'NONE', ( #2331, #18426, #4949, #4213 ) ) ;
#14937=SURFACE_STYLE_FILL_AREA ( #13040 ) ;
#14965=VECTOR ( 'NONE', #17723, 1000.000000000000000 ) ;
#14971=PLANE ( 'NONE',  #12902 ) ;
#14996=ORIENTED_EDGE ( 'NONE', *, *, #2654, .F. ) ;
#15018=AXIS2_PLACEMENT_3D ( 'NONE', #4879, #11349, #6668 ) ;
#15033=DIRECTION ( 'NONE',  ( -1.000000000000000000, -0.000000000000000000, -0.000000000000000000 ) ) ;
#15172=ADVANCED_FACE ( 'NONE', ( #3102 ), #1534, .T. ) ;
#15211=FACE_OUTER_BOUND ( 'NONE', #20583, .T. ) ;
#15231=CARTESIAN_POINT ( 'NONE',  ( 5.000000000000004441, 0.000000000000000000, 0.000000000000000000 ) ) ;
#15320=EDGE_CURVE ( 'NONE', #5544, #19012, #3612, .T. ) ;
#15388=ORIENTED_EDGE ( 'NONE', *, *, #2440, .F. ) ;
#15414=EDGE_CURVE ( 'NONE', #9241, #19897, #13801, .T. ) ;
#15422=EDGE_LOOP ( 'NONE', ( #7464, #7193 ) ) ;
#15448=ORIENTED_EDGE ( 'NONE', *, *, #11504, .F. ) ;
#15458=FACE_OUTER_BOUND ( 'NONE', #11273, .T. ) ;
#15483=LINE ( 'NONE', #16861, #8333 ) ;
#15486=CARTESIAN_POINT ( 'NONE',  ( -31.74999999999995737, 5.204748896376250699E-16, -4.250000000000000000 ) ) ;
#15504=DIRECTION ( 'NONE',  ( 0.000000000000000000, 1.224646799147353207E-16, 1.000000000000000000 ) ) ;
#15525=DIRECTION ( 'NONE',  ( 0.000000000000000000, 0.5000000000000011102, 0.8660254037844380415 ) ) ;
#15578=VECTOR ( 'NONE', #1226, 1000.000000000000000 ) ;
#15582=EDGE_CURVE ( 'NONE', #11, #13626, #4673, .T. ) ;
#15600=VERTEX_POINT ( 'NONE', #14009 ) ;
#15601=DIRECTION ( 'NONE',  ( -1.000000000000000000, -0.000000000000000000, -0.000000000000000000 ) ) ;
#15608=DIRECTION ( 'NONE',  ( -1.000000000000000000, -0.000000000000000000, -0.000000000000000000 ) ) ;
#15696=VECTOR ( 'NONE', #11073, 1000.000000000000000 ) ;
#15721=DIRECTION ( 'NONE',  ( 0.000000000000000000, -0.5000000000000011102, -0.8660254037844379305 ) ) ;
#15725=FACE_OUTER_BOUND ( 'NONE', #226, .T. ) ;
#15727=EDGE_CURVE ( 'NONE', #4659, #13626, #14432, .T. ) ;
#15817=ORIENTED_EDGE ( 'NONE', *, *, #808, .T. ) ;
#15828=EDGE_CURVE ( 'NONE', #12190, #10418, #12678, .T. ) ;
#15831=EDGE_CURVE ( 'NONE', #10418, #15600, #19418, .T. ) ;
#15867=DIRECTION ( 'NONE',  ( -1.000000000000000000, -0.000000000000000000, -0.000000000000000000 ) ) ;
#15886=ORIENTED_EDGE ( 'NONE', *, *, #10864, .F. ) ;
#16020=CARTESIAN_POINT ( 'NONE',  ( 2.500000000000000000, -1.768423874527823791, -1.020999999999998353 ) ) ;
#16023=DIRECTION ( 'NONE',  ( 0.000000000000000000, 0.000000000000000000, -1.000000000000000000 ) ) ;
#16078=ADVANCED_FACE ( 'NONE', ( #184 ), #1498, .T. ) ;
#16079=ORIENTED_EDGE ( 'NONE', *, *, #11023, .F. ) ;
#16117=AXIS2_PLACEMENT_3D ( 'NONE', #9508, #14806, #71 ) ;
#16141=VERTEX_POINT ( 'NONE', #16917 ) ;
#16164=VERTEX_POINT ( 'NONE', #2085 ) ;
#16171=VECTOR ( 'NONE', #15867, 1000.000000000000000 ) ;
#16187=ORIENTED_EDGE ( 'NONE', *, *, #11676, .F. ) ;
#16204=DIRECTION ( 'NONE',  ( 1.000000000000000000, 0.000000000000000000, 0.000000000000000000 ) ) ;
#16294=CARTESIAN_POINT ( 'NONE',  ( 2.500000000000000000, 2.357898499370433054, -1.951563910473907981E-15 ) ) ;
#16319=CIRCLE ( 'NONE', #1122, 4.000000000000000000 ) ;
#16378=CARTESIAN_POINT ( 'NONE',  ( 0.000000000000000000, 1.178949249685213863, -2.042000000000001148 ) ) ;
#16394=DIRECTION ( 'NONE',  ( -1.000000000000000000, -0.000000000000000000, -0.000000000000000000 ) ) ;
#16399=EDGE_CURVE ( 'NONE', #18355, #17230, #4515, .T. ) ;
#16406=DIRECTION ( 'NONE',  ( 0.000000000000000000, 0.000000000000000000, 1.000000000000000000 ) ) ;
#16429=CARTESIAN_POINT ( 'NONE',  ( 0.000000000000000000, -2.357898499370432610, 3.252606517456513302E-15 ) ) ;
#16449=CARTESIAN_POINT ( 'NONE',  ( 17.00000000000000000, 0.000000000000000000, 0.000000000000000000 ) ) ;
#16475=CARTESIAN_POINT ( 'NONE',  ( 17.00000000000000000, 2.789133085058097101E-16, -2.055000000000000160 ) ) ;
#16476=ADVANCED_FACE ( 'NONE', ( #4828, #17769 ), #11294, .T. ) ;
#16488=CARTESIAN_POINT ( 'NONE',  ( 0.000000000000000000, -1.178949249685213863, 2.042000000000002924 ) ) ;
#16492=ORIENTED_EDGE ( 'NONE', *, *, #15320, .T. ) ;
#16501=ADVANCED_BREP_SHAPE_REPRESENTATION ( '', ( #17543, #12461 ), #19129 ) ;
#16542=ORIENTED_EDGE ( 'NONE', *, *, #7419, .T. ) ;
#16581=DIRECTION ( 'NONE',  ( 0.000000000000000000, 1.000000000000000000, -1.224646799147353207E-16 ) ) ;
#16599=EDGE_CURVE ( 'NONE', #11681, #9241, #8147, .T. ) ;
#16601=CONICAL_SURFACE ( 'NONE', #707, 2.041999999999999815, 1.047197551196591858 ) ;
#16618=( NAMED_UNIT ( * ) SI_UNIT ( $, .STERADIAN. ) SOLID_ANGLE_UNIT ( ) );
#16669=EDGE_CURVE ( 'NONE', #2302, #19812, #364, .T. ) ;
#16696=EDGE_LOOP ( 'NONE', ( #6357, #2917, #6827, #7858, #7560 ) ) ;
#16709=CARTESIAN_POINT ( 'NONE',  ( -31.74999999999995737, 0.000000000000000000, 0.000000000000000000 ) ) ;
#16751=CARTESIAN_POINT ( 'NONE',  ( 5.200000000000002842, 3.061616997868383634E-16, -2.500000000000000444 ) ) ;
#16806=CIRCLE ( 'NONE', #4960, 2.055000000000000160 ) ;
#16828=VECTOR ( 'NONE', #2093, 1000.000000000000114 ) ;
#16850=EDGE_CURVE ( 'NONE', #19897, #13895, #7564, .T. ) ;
#16861=CARTESIAN_POINT ( 'NONE',  ( -31.74999999999995737, 0.000000000000000000, 2.500000000000000444 ) ) ;
#16917=CARTESIAN_POINT ( 'NONE',  ( 2.500000000000000000, 1.768423874527822681, -1.021000000000002794 ) ) ;
#16929=EDGE_CURVE ( 'NONE', #17230, #10641, #14565, .T. ) ;
#16950=DIRECTION ( 'NONE',  ( 0.000000000000000000, 0.000000000000000000, -1.000000000000000000 ) ) ;
#17052=VECTOR ( 'NONE', #13569, 1000.000000000000000 ) ;
#17117=FACE_OUTER_BOUND ( 'NONE', #17760, .T. ) ;
#17225=CARTESIAN_POINT ( 'NONE',  ( 17.00000000000000000, 0.000000000000000000, 2.055000000000000160 ) ) ;
#17230=VERTEX_POINT ( 'NONE', #2565 ) ;
#17252=APPLICATION_CONTEXT ( 'automotive_design' ) ;
#17262=FACE_OUTER_BOUND ( 'NONE', #18822, .T. ) ;
#17294=VECTOR ( 'NONE', #5436, 1000.000000000000114 ) ;
#17326=ORIENTED_EDGE ( 'NONE', *, *, #537, .T. ) ;
#17394=EDGE_LOOP ( 'NONE', ( #14186, #18815, #17326, #3700 ) ) ;
#17414=DIRECTION ( 'NONE',  ( -0.000000000000000000, 1.000000000000000000, 1.224646799147353207E-16 ) ) ;
#17419=CARTESIAN_POINT ( 'NONE',  ( 0.000000000000000000, -1.178949249685213863, 2.042000000000002924 ) ) ;
#17422=DIRECTION ( 'NONE',  ( 0.000000000000000000, 0.000000000000000000, -1.000000000000000000 ) ) ;
#17432=DIRECTION ( 'NONE',  ( 0.000000000000000000, 0.4999999999999993894, -0.8660254037844389297 ) ) ;
#17458=CARTESIAN_POINT ( 'NONE',  ( 2.500000000000000000, 2.357898499370433054, -1.951563910473907981E-15 ) ) ;
#17495=CONICAL_SURFACE ( 'NONE', #8338, 2.041999999999999815, 1.047197551196591858 ) ;
#17508=DIRECTION ( 'NONE',  ( 0.000000000000000000, -0.5000000000000012212, -0.8660254037844380415 ) ) ;
#17510=ADVANCED_FACE ( 'NONE', ( #6115, #15458 ), #7494, .T. ) ;
#17530=CARTESIAN_POINT ( 'NONE',  ( 2.500000000000000000, 2.357898499370433054, -1.951563910473907981E-15 ) ) ;
#17540=ORIENTED_EDGE ( 'NONE', *, *, #20402, .T. ) ;
#17543=MANIFOLD_SOLID_BREP ( 'Hex', #5831 ) ;
#17636=AXIS2_PLACEMENT_3D ( 'NONE', #13584, #5411, #11995 ) ;
#17642=VERTEX_POINT ( 'NONE', #18837 ) ;
#17665=LINE ( 'NONE', #11193, #19284 ) ;
#17723=DIRECTION ( 'NONE',  ( 0.000000000000000000, 1.000000000000000000, -1.471414886128461471E-15 ) ) ;
#17724=EDGE_LOOP ( 'NONE', ( #18764, #16187, #8412, #397, #11549, #19057 ) ) ;
#17760=EDGE_LOOP ( 'NONE', ( #14996, #8197, #11281, #20276, #5111 ) ) ;
#17769=FACE_OUTER_BOUND ( 'NONE', #11584, .T. ) ;
#17779=EDGE_CURVE ( 'NONE', #11144, #14849, #17665, .T. ) ;
#17805=CARTESIAN_POINT ( 'NONE',  ( 0.000000000000000000, -2.357898499370432610, 3.252606517456513302E-15 ) ) ;
#17815=CIRCLE ( 'NONE', #16117, 2.041999999999999815 ) ;
#17838=CIRCLE ( 'NONE', #3918, 2.500000000000000444 ) ;
#17869=AXIS2_PLACEMENT_3D ( 'NONE', #17530, #12436, #17422 ) ;
#17928=LINE ( 'NONE', #6156, #14965 ) ;
#17930=DIRECTION ( 'NONE',  ( 1.000000000000000000, 0.000000000000000000, 0.000000000000000000 ) ) ;
#17959=VECTOR ( 'NONE', #9879, 1000.000000000000114 ) ;
#17983=CARTESIAN_POINT ( 'NONE',  ( 2.500000000000000000, 2.357898499370433054, -1.951563910473907981E-15 ) ) ;
#18001=CIRCLE ( 'NONE', #1760, 0.2500000000000002220 ) ;
#18039=AXIS2_PLACEMENT_3D ( 'NONE', #400, #6853, #16406 ) ;
#18062=DIRECTION ( 'NONE',  ( 0.000000000000000000, -0.5000000000000012212, -0.8660254037844380415 ) ) ;
#18084=ORIENTED_EDGE ( 'NONE', *, *, #11962, .F. ) ;
#18112=EDGE_CURVE ( 'NONE', #4659, #14903, #11169, .T. ) ;
#18158=CARTESIAN_POINT ( 'NONE',  ( 0.2500000000000002220, 5.204748896376250699E-16, -4.250000000000000000 ) ) ;
#18245=DIRECTION ( 'NONE',  ( -0.7071067811865369146, 8.659560562355062281E-17, -0.7071067811865582309 ) ) ;
#18262=DIRECTION ( 'NONE',  ( 0.000000000000000000, 0.000000000000000000, -1.000000000000000000 ) ) ;
#18267=( LENGTH_UNIT ( ) NAMED_UNIT ( * ) SI_UNIT ( .MILLI., .METRE. ) );
#18303=VECTOR ( 'NONE', #13264, 1000.000000000000000 ) ;
#18353=CARTESIAN_POINT ( 'NONE',  ( 2.500000000000000000, 2.357898499370433054, -1.951563910473907981E-15 ) ) ;
#18355=VERTEX_POINT ( 'NONE', #18353 ) ;
#18367=TOROIDAL_SURFACE ( 'NONE', #2447, 2.700000000000000622, 0.2000000000000000111 ) ;
#18369=ADVANCED_FACE ( 'NONE', ( #4141 ), #10509, .F. ) ;
#18373=DIRECTION ( 'NONE',  ( -1.000000000000000000, -0.000000000000000000, -0.000000000000000000 ) ) ;
#18379=ORIENTED_EDGE ( 'NONE', *, *, #15831, .F. ) ;
#18421=DIRECTION ( 'NONE',  ( 1.000000000000000000, 0.000000000000000000, 0.000000000000000000 ) ) ;
#18426=ORIENTED_EDGE ( 'NONE', *, *, #537, .F. ) ;
#18446=LINE ( 'NONE', #2021, #8237 ) ;
#18454=ADVANCED_FACE ( 'NONE', ( #10412 ), #14971, .F. ) ;
#18469=VERTEX_POINT ( 'NONE', #4031 ) ;
#18564=ORIENTED_EDGE ( 'NONE', *, *, #8713, .T. ) ;
#18583=ORIENTED_EDGE ( 'NONE', *, *, #954, .F. ) ;
#18651=EDGE_CURVE ( 'NONE', #18355, #5544, #6568, .T. ) ;
#18664=AXIS2_PLACEMENT_3D ( 'NONE', #8294, #12977, #13079 ) ;
#18691=DIRECTION ( 'NONE',  ( -1.000000000000000000, -0.000000000000000000, -0.000000000000000000 ) ) ;
#18729=VECTOR ( 'NONE', #18245, 1000.000000000000000 ) ;
#18762=CARTESIAN_POINT ( 'NONE',  ( 2.500000000000000000, 1.178949249685218525, 2.041999999999999371 ) ) ;
#18764=ORIENTED_EDGE ( 'NONE', *, *, #16929, .T. ) ;
#18813=PLANE ( 'NONE',  #12294 ) ;
#18815=ORIENTED_EDGE ( 'NONE', *, *, #16850, .T. ) ;
#18822=EDGE_LOOP ( 'NONE', ( #10817, #14360, #13282 ) ) ;
#18837=CARTESIAN_POINT ( 'NONE',  ( 2.500000000000000000, -1.768423874527823569, 1.021000000000002794 ) ) ;
#18906=CARTESIAN_POINT ( 'NONE',  ( 2.500000000000000000, 0.000000000000000000, 0.000000000000000000 ) ) ;
#18914=CARTESIAN_POINT ( 'NONE',  ( 2.500000000000000000, 2.357898499370433054, -1.951563910473907981E-15 ) ) ;
#18975=CARTESIAN_POINT ( 'NONE',  ( 5.000000000000000888, 0.000000000000000000, 0.000000000000000000 ) ) ;
#18992=CARTESIAN_POINT ( 'NONE',  ( 2.500000000000000000, -1.178949249685213863, 2.042000000000002924 ) ) ;
#19012=VERTEX_POINT ( 'NONE', #18762 ) ;
#19019=ORIENTED_EDGE ( 'NONE', *, *, #38, .F. ) ;
#19034=DIRECTION ( 'NONE',  ( -1.000000000000000000, -0.000000000000000000, -0.000000000000000000 ) ) ;
#19056=CIRCLE ( 'NONE', #7187, 4.250000000000000000 ) ;
#19057=ORIENTED_EDGE ( 'NONE', *, *, #10028, .F. ) ;
#19129=( GEOMETRIC_REPRESENTATION_CONTEXT ( 3 ) GLOBAL_UNCERTAINTY_ASSIGNED_CONTEXT ( ( #313 ) ) GLOBAL_UNIT_ASSIGNED_CONTEXT ( ( #19598, #4983, #10162 ) ) REPRESENTATION_CONTEXT ( 'NONE', 'WORKASPACE' ) );
#19131=DIRECTION ( 'NONE',  ( -0.7071067811865369146, 0.000000000000000000, 0.7071067811865582309 ) ) ;
#19135=DIRECTION ( 'NONE',  ( -1.000000000000000000, -0.000000000000000000, -0.000000000000000000 ) ) ;
#19169=EDGE_LOOP ( 'NONE', ( #20144, #3376, #4718, #6267, #17540 ) ) ;
#19197=EDGE_CURVE ( 'NONE', #1468, #19897, #8705, .T. ) ;
#19249=DIRECTION ( 'NONE',  ( 0.000000000000000000, 1.000000000000000000, -1.471414886128461471E-15 ) ) ;
#19250=DIRECTION ( 'NONE',  ( 0.000000000000000000, -1.000000000000000000, 1.287488025362403787E-15 ) ) ;
#19284=VECTOR ( 'NONE', #19249, 1000.000000000000000 ) ;
#19293=ORIENTED_EDGE ( 'NONE', *, *, #11538, .T. ) ;
#19312=AXIS2_PLACEMENT_3D ( 'NONE', #10119, #13415, #13721 ) ;
#19336=ADVANCED_FACE ( 'NONE', ( #17117 ), #2603, .T. ) ;
#19351=DIRECTION ( 'NONE',  ( -1.000000000000000000, -0.000000000000000000, -0.000000000000000000 ) ) ;
#19363=PLANE ( 'NONE',  #14630 ) ;
#19411=CARTESIAN_POINT ( 'NONE',  ( 0.2500000000000002220, 0.000000000000000000, 0.000000000000000000 ) ) ;
#19418=CIRCLE ( 'NONE', #15018, 0.2500000000000002220 ) ;
#19474=CARTESIAN_POINT ( 'NONE',  ( 0.000000000000000000, 0.000000000000000000, 0.000000000000000000 ) ) ;
#19495=( LENGTH_UNIT ( ) NAMED_UNIT ( * ) SI_UNIT ( .MILLI., .METRE. ) );
#19557=VERTEX_POINT ( 'NONE', #4500 ) ;
#19582=PRODUCT_DEFINITION ( 'UNKNOWN', '', #13716, #7075 ) ;
#19598=( LENGTH_UNIT ( ) NAMED_UNIT ( * ) SI_UNIT ( .MILLI., .METRE. ) );
#19613=FACE_OUTER_BOUND ( 'NONE', #8779, .T. ) ;
#19638=LINE ( 'NONE', #5115, #13465 ) ;
#19653=DIRECTION ( 'NONE',  ( 0.000000000000000000, 0.000000000000000000, 1.000000000000000000 ) ) ;
#19677=DIRECTION ( 'NONE',  ( 0.000000000000000000, 0.4999999999999993339, -0.8660254037844390407 ) ) ;
#19716=CARTESIAN_POINT ( 'NONE',  ( 2.500000000000000000, -2.357898499370432610, 3.252606517456513302E-15 ) ) ;
#19734=TOROIDAL_SURFACE ( 'NONE', #12989, 4.000000000000000000, 0.2500000000000000000 ) ;
#19786=ORIENTED_EDGE ( 'NONE', *, *, #18651, .F. ) ;
#19797=CARTESIAN_POINT ( 'NONE',  ( 2.500000000000000000, -2.357898499370432610, 3.252606517456513302E-15 ) ) ;
#19798=DIRECTION ( 'NONE',  ( 0.000000000000000000, 0.000000000000000000, 1.000000000000000000 ) ) ;
#19812=VERTEX_POINT ( 'NONE', #17805 ) ;
#19822=DIRECTION ( 'NONE',  ( -1.000000000000000000, -0.000000000000000000, -0.000000000000000000 ) ) ;
#19843=ADVANCED_FACE ( 'NONE', ( #8290 ), #193, .F. ) ;
#19850=CARTESIAN_POINT ( 'NONE',  ( 5.000000000000000888, 0.000000000000000000, 0.000000000000000000 ) ) ;
#19851=AXIS2_PLACEMENT_3D ( 'NONE', #746, #19822, #13683 ) ;
#19897=VERTEX_POINT ( 'NONE', #11522 ) ;
#19912=DIRECTION ( 'NONE',  ( 0.000000000000000000, 0.000000000000000000, -1.000000000000000000 ) ) ;
#20046=VECTOR ( 'NONE', #1994, 999.9999999999998863 ) ;
#20144=ORIENTED_EDGE ( 'NONE', *, *, #15582, .F. ) ;
#20214=ORIENTED_EDGE ( 'NONE', *, *, #5905, .F. ) ;
#20217=EDGE_CURVE ( 'NONE', #5544, #16141, #4648, .T. ) ;
#20276=ORIENTED_EDGE ( 'NONE', *, *, #1702, .T. ) ;
#20284=EDGE_LOOP ( 'NONE', ( #7092, #9472, #15448 ) ) ;
#20363=COLOUR_RGB ( '', 0.31764706, 0.68627451, 0.89019608) ;
#20366=ORIENTED_EDGE ( 'NONE', *, *, #954, .T. ) ;
#20367=EDGE_CURVE ( 'NONE', #14604, #3608, #11408, .T. ) ;
#20373=AXIS2_PLACEMENT_3D ( 'NONE', #10772, #13523, #15525 ) ;
#20376=LINE ( 'NONE', #14038, #217 ) ;
#20378=LINE ( 'NONE', #10648, #3850 ) ;
#20402=EDGE_CURVE ( 'NONE', #16141, #13626, #6004, .T. ) ;
#20412=AXIS2_PLACEMENT_3D ( 'NONE', #4448, #12515, #12300 ) ;
#20442=UNCERTAINTY_MEASURE_WITH_UNIT (LENGTH_MEASURE( 1.000000000000000082E-05 ), #18267, 'distance_accuracy_value', 'NONE');
#20447=AXIS2_PLACEMENT_3D ( 'NONE', #4274, #15608, #1111 ) ;
#20482=CARTESIAN_POINT ( 'NONE',  ( 2.500000000000000000, -2.629050547790028551E-15, -2.041999999999999815 ) ) ;
#20499=CARTESIAN_POINT ( 'NONE',  ( 2.500000000000000000, -1.178949249685218303, -2.041999999999998039 ) ) ;
#20571=ADVANCED_FACE ( 'NONE', ( #4588 ), #9558, .F. ) ;
#20583=EDGE_LOOP ( 'NONE', ( #3472, #18583, #2605, #10744, #16542 ) ) ;
#20590=ORIENTED_EDGE ( 'NONE', *, *, #1009, .T. ) ;
#20595=PLANE ( 'NONE',  #9282 ) ;
#20601=CARTESIAN_POINT ( 'NONE',  ( 2.500000000000000000, 2.357898499370433054, -1.951563910473907981E-15 ) ) ;
#20631=EDGE_LOOP ( 'NONE', ( #4239, #12211, #8893 ) ) ;
#20653=ORIENTED_EDGE ( 'NONE', *, *, #5905, .T. ) ;
#20694=CARTESIAN_POINT ( 'NONE',  ( 0.000000000000000000, 2.357898499370433054, -1.951563910473907981E-15 ) ) ;
#20834=DIRECTION ( 'NONE',  ( 0.000000000000000000, 0.000000000000000000, 1.000000000000000000 ) ) ;
#20848=DIRECTION ( 'NONE',  ( 0.000000000000000000, -1.000000000000000000, 1.471414886128461471E-15 ) ) ;
#20852=STYLED_ITEM ( 'NONE', ( #6865 ), #16501 ) ;
#20916=ADVANCED_FACE ( 'NONE', ( #3669 ), #11625, .T. ) ;
#20932=DIRECTION ( 'NONE',  ( -0.000000000000000000, 0.000000000000000000, 1.000000000000000000 ) ) ;
#20937=DIRECTION ( 'NONE',  ( 0.000000000000000000, 0.000000000000000000, 1.000000000000000000 ) ) ;
ENDSEC;
END-ISO-10303-21;
